ISO-10303-21;
HEADER;
/* Generated by software containing ST-Developer
 * from STEP Tools, Inc. (www.steptools.com) 
 */

FILE_DESCRIPTION(
/* description */ ('Turntable on roller ring'),
/* implementation_level */ '2;1');

FILE_NAME(
/* name */ 'Outer ring (1).step',
/* time_stamp */ '2026-10-28T03:23:59-07:00',
/* author */ (''),
/* organization */ (''),
/* preprocessor_version */ 'ST-DEVELOPER v20.2',
/* originating_system */ 'Autodesk Translation Framework v15.17.0.0',
/* authorisation */ '');

FILE_SCHEMA (('AUTOMOTIVE_DESIGN { 1 0 10303 214 3 1 1 }'));
ENDSEC;

DATA;
#10=MECHANICAL_DESIGN_GEOMETRIC_PRESENTATION_REPRESENTATION('',(#677),#16281);
#475=TOROIDAL_SURFACE('',#10062,1.,0.247676);
#497=CONICAL_SURFACE('',#10073,1.47,0.785398163397449);
#498=CONICAL_SURFACE('',#10077,1.47,0.785398163397449);
#558=SHAPE_REPRESENTATION_RELATIONSHIP('SRR','None',#16583,#613);
#613=ADVANCED_BREP_SHAPE_REPRESENTATION('',(#745),#16277);
#677=STYLED_ITEM('',(#16932),#745);
#745=MANIFOLD_SOLID_BREP('Body1',#8422);
#983=FACE_BOUND('',#2446,.T.);
#984=FACE_BOUND('',#2451,.T.);
#1235=PLANE('',#10070);
#1236=PLANE('',#10079);
#1712=FACE_OUTER_BOUND('',#2443,.T.);
#1713=FACE_OUTER_BOUND('',#2444,.T.);
#1714=FACE_OUTER_BOUND('',#2445,.T.);
#1715=FACE_OUTER_BOUND('',#2447,.T.);
#1716=FACE_OUTER_BOUND('',#2448,.T.);
#1717=FACE_OUTER_BOUND('',#2449,.T.);
#1718=FACE_OUTER_BOUND('',#2450,.T.);
#1719=FACE_OUTER_BOUND('',#2452,.T.);
#2443=EDGE_LOOP('',(#7489,#7490,#7491,#7492,#7493,#7494));
#2444=EDGE_LOOP('',(#7495,#7496,#7497,#7498,#7499));
#2445=EDGE_LOOP('',(#7500));
#2446=EDGE_LOOP('',(#7501));
#2447=EDGE_LOOP('',(#7502,#7503,#7504,#7505));
#2448=EDGE_LOOP('',(#7506,#7507,#7508,#7509));
#2449=EDGE_LOOP('',(#7510,#7511,#7512,#7513));
#2450=EDGE_LOOP('',(#7514));
#2451=EDGE_LOOP('',(#7515));
#2452=EDGE_LOOP('',(#7516,#7517,#7518,#7519,#7520));
#2965=LINE('',#15582,#3448);
#2966=LINE('',#15591,#3449);
#2967=LINE('',#15595,#3450);
#2968=LINE('',#15599,#3451);
#2969=LINE('',#15602,#3452);
#3448=VECTOR('',#12732,1.023815);
#3449=VECTOR('',#12743,1.47);
#3450=VECTOR('',#12748,1.5);
#3451=VECTOR('',#12753,1.47);
#3452=VECTOR('',#12758,1.023815);
#3888=CIRCLE('',#10063,1.023815);
#3889=CIRCLE('',#10064,1.023815);
#3890=CIRCLE('',#10065,0.247676);
#3891=CIRCLE('',#10066,1.023815);
#3892=CIRCLE('',#10067,1.023815);
#3893=CIRCLE('',#10069,1.023815);
#3894=CIRCLE('',#10071,1.44);
#3895=CIRCLE('',#10072,1.023815);
#3896=CIRCLE('',#10074,1.5);
#3897=CIRCLE('',#10076,1.5);
#3898=CIRCLE('',#10078,1.44);
#4563=VERTEX_POINT('',#15570);
#4564=VERTEX_POINT('',#15571);
#4565=VERTEX_POINT('',#15574);
#4566=VERTEX_POINT('',#15576);
#4567=VERTEX_POINT('',#15580);
#4568=VERTEX_POINT('',#15584);
#4569=VERTEX_POINT('',#15586);
#4570=VERTEX_POINT('',#15589);
#4571=VERTEX_POINT('',#15593);
#4572=VERTEX_POINT('',#15597);
#5555=EDGE_CURVE('',#4563,#4564,#3888,.T.);
#5556=EDGE_CURVE('',#4564,#4563,#3889,.T.);
#5557=EDGE_CURVE('',#4564,#4565,#3890,.T.);
#5558=EDGE_CURVE('',#4566,#4565,#3891,.T.);
#5559=EDGE_CURVE('',#4565,#4566,#3892,.T.);
#5560=EDGE_CURVE('',#4567,#4567,#3893,.T.);
#5561=EDGE_CURVE('',#4567,#4566,#2965,.T.);
#5562=EDGE_CURVE('',#4568,#4568,#3894,.T.);
#5563=EDGE_CURVE('',#4569,#4569,#3895,.T.);
#5564=EDGE_CURVE('',#4570,#4570,#3896,.T.);
#5565=EDGE_CURVE('',#4570,#4568,#2966,.T.);
#5566=EDGE_CURVE('',#4571,#4571,#3897,.T.);
#5567=EDGE_CURVE('',#4571,#4570,#2967,.T.);
#5568=EDGE_CURVE('',#4572,#4572,#3898,.T.);
#5569=EDGE_CURVE('',#4572,#4571,#2968,.T.);
#5570=EDGE_CURVE('',#4563,#4569,#2969,.T.);
#7489=ORIENTED_EDGE('',*,*,#5555,.F.);
#7490=ORIENTED_EDGE('',*,*,#5556,.F.);
#7491=ORIENTED_EDGE('',*,*,#5557,.T.);
#7492=ORIENTED_EDGE('',*,*,#5558,.F.);
#7493=ORIENTED_EDGE('',*,*,#5559,.F.);
#7494=ORIENTED_EDGE('',*,*,#5557,.F.);
#7495=ORIENTED_EDGE('',*,*,#5560,.T.);
#7496=ORIENTED_EDGE('',*,*,#5561,.T.);
#7497=ORIENTED_EDGE('',*,*,#5558,.T.);
#7498=ORIENTED_EDGE('',*,*,#5559,.T.);
#7499=ORIENTED_EDGE('',*,*,#5561,.F.);
#7500=ORIENTED_EDGE('',*,*,#5562,.F.);
#7501=ORIENTED_EDGE('',*,*,#5563,.T.);
#7502=ORIENTED_EDGE('',*,*,#5564,.F.);
#7503=ORIENTED_EDGE('',*,*,#5565,.T.);
#7504=ORIENTED_EDGE('',*,*,#5562,.T.);
#7505=ORIENTED_EDGE('',*,*,#5565,.F.);
#7506=ORIENTED_EDGE('',*,*,#5566,.F.);
#7507=ORIENTED_EDGE('',*,*,#5567,.T.);
#7508=ORIENTED_EDGE('',*,*,#5564,.T.);
#7509=ORIENTED_EDGE('',*,*,#5567,.F.);
#7510=ORIENTED_EDGE('',*,*,#5568,.F.);
#7511=ORIENTED_EDGE('',*,*,#5569,.T.);
#7512=ORIENTED_EDGE('',*,*,#5566,.T.);
#7513=ORIENTED_EDGE('',*,*,#5569,.F.);
#7514=ORIENTED_EDGE('',*,*,#5568,.T.);
#7515=ORIENTED_EDGE('',*,*,#5560,.F.);
#7516=ORIENTED_EDGE('',*,*,#5555,.T.);
#7517=ORIENTED_EDGE('',*,*,#5556,.T.);
#7518=ORIENTED_EDGE('',*,*,#5570,.T.);
#7519=ORIENTED_EDGE('',*,*,#5563,.F.);
#7520=ORIENTED_EDGE('',*,*,#5570,.F.);
#7844=CYLINDRICAL_SURFACE('',#10068,1.023815);
#7845=CYLINDRICAL_SURFACE('',#10075,1.5);
#7846=CYLINDRICAL_SURFACE('',#10080,1.023815);
#8315=ADVANCED_FACE('',(#1712),#475,.F.);
#8316=ADVANCED_FACE('',(#1713),#7844,.F.);
#8317=ADVANCED_FACE('',(#1714,#983),#1235,.T.);
#8318=ADVANCED_FACE('',(#1715),#497,.T.);
#8319=ADVANCED_FACE('',(#1716),#7845,.T.);
#8320=ADVANCED_FACE('',(#1717),#498,.T.);
#8321=ADVANCED_FACE('',(#1718,#984),#1236,.T.);
#8322=ADVANCED_FACE('',(#1719),#7846,.F.);
#8422=CLOSED_SHELL('',(#8315,#8316,#8317,#8318,#8319,#8320,#8321,#8322));
#10061=AXIS2_PLACEMENT_3D('',#15568,#12714,#12715);
#10062=AXIS2_PLACEMENT_3D('',#15569,#12716,#12717);
#10063=AXIS2_PLACEMENT_3D('',#15572,#12718,#12719);
#10064=AXIS2_PLACEMENT_3D('',#15573,#12720,#12721);
#10065=AXIS2_PLACEMENT_3D('',#15575,#12722,#12723);
#10066=AXIS2_PLACEMENT_3D('',#15577,#12724,#12725);
#10067=AXIS2_PLACEMENT_3D('',#15578,#12726,#12727);
#10068=AXIS2_PLACEMENT_3D('',#15579,#12728,#12729);
#10069=AXIS2_PLACEMENT_3D('',#15581,#12730,#12731);
#10070=AXIS2_PLACEMENT_3D('',#15583,#12733,#12734);
#10071=AXIS2_PLACEMENT_3D('',#15585,#12735,#12736);
#10072=AXIS2_PLACEMENT_3D('',#15587,#12737,#12738);
#10073=AXIS2_PLACEMENT_3D('',#15588,#12739,#12740);
#10074=AXIS2_PLACEMENT_3D('',#15590,#12741,#12742);
#10075=AXIS2_PLACEMENT_3D('',#15592,#12744,#12745);
#10076=AXIS2_PLACEMENT_3D('',#15594,#12746,#12747);
#10077=AXIS2_PLACEMENT_3D('',#15596,#12749,#12750);
#10078=AXIS2_PLACEMENT_3D('',#15598,#12751,#12752);
#10079=AXIS2_PLACEMENT_3D('',#15600,#12754,#12755);
#10080=AXIS2_PLACEMENT_3D('',#15601,#12756,#12757);
#12714=DIRECTION('axis',(0.,0.,1.));
#12715=DIRECTION('refdir',(1.,0.,0.));
#12716=DIRECTION('center_axis',(0.,-1.,0.));
#12717=DIRECTION('ref_axis',(0.,0.,-1.));
#12718=DIRECTION('center_axis',(0.,-1.,0.));
#12719=DIRECTION('ref_axis',(1.,0.,0.));
#12720=DIRECTION('center_axis',(0.,-1.,0.));
#12721=DIRECTION('ref_axis',(1.,0.,0.));
#12722=DIRECTION('center_axis',(1.,0.,1.22464679914735E-16));
#12723=DIRECTION('ref_axis',(-1.22464679914735E-16,0.,1.));
#12724=DIRECTION('center_axis',(0.,1.,0.));
#12725=DIRECTION('ref_axis',(1.,0.,0.));
#12726=DIRECTION('center_axis',(0.,1.,0.));
#12727=DIRECTION('ref_axis',(1.,0.,0.));
#12728=DIRECTION('center_axis',(0.,-1.,0.));
#12729=DIRECTION('ref_axis',(1.,0.,0.));
#12730=DIRECTION('center_axis',(0.,-1.,0.));
#12731=DIRECTION('ref_axis',(1.,0.,0.));
#12732=DIRECTION('',(0.,1.,0.));
#12733=DIRECTION('center_axis',(0.,1.,0.));
#12734=DIRECTION('ref_axis',(0.,0.,1.));
#12735=DIRECTION('center_axis',(0.,-1.,0.));
#12736=DIRECTION('ref_axis',(1.,0.,0.));
#12737=DIRECTION('center_axis',(0.,-1.,0.));
#12738=DIRECTION('ref_axis',(1.,0.,0.));
#12739=DIRECTION('center_axis',(0.,-1.,0.));
#12740=DIRECTION('ref_axis',(1.,0.,0.));
#12741=DIRECTION('center_axis',(0.,-1.,0.));
#12742=DIRECTION('ref_axis',(1.,0.,0.));
#12743=DIRECTION('',(0.707106781186548,0.707106781186547,8.65956056235494E-17));
#12744=DIRECTION('center_axis',(0.,-1.,0.));
#12745=DIRECTION('ref_axis',(1.,0.,0.));
#12746=DIRECTION('center_axis',(0.,-1.,0.));
#12747=DIRECTION('ref_axis',(1.,0.,0.));
#12748=DIRECTION('',(0.,1.,0.));
#12749=DIRECTION('center_axis',(0.,1.,0.));
#12750=DIRECTION('ref_axis',(1.,0.,0.));
#12751=DIRECTION('center_axis',(0.,-1.,0.));
#12752=DIRECTION('ref_axis',(1.,0.,0.));
#12753=DIRECTION('',(-0.707106781186548,0.707106781186547,-8.65956056235494E-17));
#12754=DIRECTION('center_axis',(0.,-1.,0.));
#12755=DIRECTION('ref_axis',(0.,0.,-1.));
#12756=DIRECTION('center_axis',(0.,-1.,0.));
#12757=DIRECTION('ref_axis',(1.,0.,0.));
#12758=DIRECTION('',(0.,1.,0.));
#15568=CARTESIAN_POINT('',(0.,0.,0.));
#15569=CARTESIAN_POINT('Origin',(0.,0.,0.));
#15570=CARTESIAN_POINT('',(-1.023815,0.246528389340863,-1.25381176266905E-16));
#15571=CARTESIAN_POINT('',(-1.25381176266905E-16,0.246528389340863,1.023815));
#15572=CARTESIAN_POINT('Origin',(0.,0.246528389340863,0.));
#15573=CARTESIAN_POINT('Origin',(0.,0.246528389340863,0.));
#15574=CARTESIAN_POINT('',(-1.25381176266905E-16,-0.246528389340863,1.023815));
#15575=CARTESIAN_POINT('Origin',(-1.22464679914735E-16,0.,1.));
#15576=CARTESIAN_POINT('',(-1.023815,-0.246528389340863,1.25381176266905E-16));
#15577=CARTESIAN_POINT('Origin',(0.,-0.246528389340863,0.));
#15578=CARTESIAN_POINT('Origin',(0.,-0.246528389340863,0.));
#15579=CARTESIAN_POINT('Origin',(0.,0.,0.));
#15580=CARTESIAN_POINT('',(-1.023815,-0.45,-1.25381176266905E-16));
#15581=CARTESIAN_POINT('Origin',(0.,-0.45,0.));
#15582=CARTESIAN_POINT('',(-1.023815,0.,-1.25381176266905E-16));
#15583=CARTESIAN_POINT('Origin',(1.44,0.45,0.));
#15584=CARTESIAN_POINT('',(-1.44,0.45,-1.76349139077219E-16));
#15585=CARTESIAN_POINT('Origin',(0.,0.45,0.));
#15586=CARTESIAN_POINT('',(-1.023815,0.45,-1.25381176266905E-16));
#15587=CARTESIAN_POINT('Origin',(0.,0.45,0.));
#15588=CARTESIAN_POINT('Origin',(0.,0.42,0.));
#15589=CARTESIAN_POINT('',(-1.5,0.39,-1.83697019872103E-16));
#15590=CARTESIAN_POINT('Origin',(0.,0.39,0.));
#15591=CARTESIAN_POINT('',(-1.47,0.42,-1.80023079474661E-16));
#15592=CARTESIAN_POINT('Origin',(0.,0.,0.));
#15593=CARTESIAN_POINT('',(-1.5,-0.39,-1.83697019872103E-16));
#15594=CARTESIAN_POINT('Origin',(0.,-0.39,0.));
#15595=CARTESIAN_POINT('',(-1.5,0.,-1.83697019872103E-16));
#15596=CARTESIAN_POINT('Origin',(0.,-0.42,0.));
#15597=CARTESIAN_POINT('',(-1.44,-0.45,-1.76349139077219E-16));
#15598=CARTESIAN_POINT('Origin',(0.,-0.45,0.));
#15599=CARTESIAN_POINT('',(-1.47,-0.42,-1.80023079474661E-16));
#15600=CARTESIAN_POINT('Origin',(1.023815,-0.45,0.));
#15601=CARTESIAN_POINT('Origin',(0.,0.,0.));
#15602=CARTESIAN_POINT('',(-1.023815,0.,-1.25381176266905E-16));
#16208=UNCERTAINTY_MEASURE_WITH_UNIT(LENGTH_MEASURE(0.001),#16282,
'DISTANCE_ACCURACY_VALUE',
'Maximum model space distance between geometric entities at asserted c
onnectivities');
#16212=UNCERTAINTY_MEASURE_WITH_UNIT(LENGTH_MEASURE(0.001),#16282,
'DISTANCE_ACCURACY_VALUE',
'Maximum model space distance between geometric entities at asserted c
onnectivities');
#16277=(
GEOMETRIC_REPRESENTATION_CONTEXT(3)
GLOBAL_UNCERTAINTY_ASSIGNED_CONTEXT((#16208))
GLOBAL_UNIT_ASSIGNED_CONTEXT((#16282,#16284,#16285))
REPRESENTATION_CONTEXT('','3D')
);
#16281=(
GEOMETRIC_REPRESENTATION_CONTEXT(3)
GLOBAL_UNCERTAINTY_ASSIGNED_CONTEXT((#16212))
GLOBAL_UNIT_ASSIGNED_CONTEXT((#16282,#16284,#16285))
REPRESENTATION_CONTEXT('','3D')
);
#16282=(
LENGTH_UNIT()
NAMED_UNIT(*)
SI_UNIT(.CENTI.,.METRE.)
);
#16284=(
NAMED_UNIT(*)
PLANE_ANGLE_UNIT()
SI_UNIT($,.RADIAN.)
);
#16285=(
NAMED_UNIT(*)
SI_UNIT($,.STERADIAN.)
SOLID_ANGLE_UNIT()
);
#16350=SHAPE_DEFINITION_REPRESENTATION(#16484,#16583);
#16484=PRODUCT_DEFINITION_SHAPE('',$,#16652);
#16583=SHAPE_REPRESENTATION('',(#10061),#16277);
#16587=PRODUCT_DEFINITION_CONTEXT('part definition',#16793,'design');
#16652=PRODUCT_DEFINITION('Outer ring (1)','Outer ring (1)',#16720,#16587);
#16720=PRODUCT_DEFINITION_FORMATION('',$,#16859);
#16793=APPLICATION_CONTEXT(
'Core Data for Automotive Mechanical Design Process');
#16794=PRODUCT_CONTEXT('part definition',#16793,'mechanical');
#16859=PRODUCT('Outer ring (1)','Outer ring (1)','Outer ring (1)',(#16794));
#16926=COLOUR_RGB('Grey',0.48,0.52,0.57);
#16927=FILL_AREA_STYLE_COLOUR('',#16926);
#16928=FILL_AREA_STYLE('',(#16927));
#16929=SURFACE_STYLE_FILL_AREA(#16928);
#16930=SURFACE_SIDE_STYLE('',(#16929));
#16931=SURFACE_STYLE_USAGE(.BOTH.,#16930);
#16932=PRESENTATION_STYLE_ASSIGNMENT((#16931));
ENDSEC;
END-ISO-10303-21;
